ISO-10303-21;
HEADER;
/* Generated by software containing ST-Developer
 * from STEP Tools, Inc. (www.steptools.com) 
 */

FILE_DESCRIPTION(
/* description */ (''),
/* implementation_level */ '2;1');

FILE_NAME(
/* name */ 'Pivot thrust washer.step',
/* time_stamp */ '2026-11-10T09:09:39-08:00',
/* author */ (''),
/* organization */ (''),
/* preprocessor_version */ 'ST-DEVELOPER v20.2',
/* originating_system */ 'Autodesk Translation Framework v15.17.0.0',
/* authorisation */ '');

FILE_SCHEMA (('AUTOMOTIVE_DESIGN { 1 0 10303 214 3 1 1 }'));
ENDSEC;

DATA;
#10=MECHANICAL_DESIGN_GEOMETRIC_PRESENTATION_REPRESENTATION('',(#563),#18353);
#545=SHAPE_REPRESENTATION_RELATIONSHIP('SRR','None',#18406,#554);
#554=ADVANCED_BREP_SHAPE_REPRESENTATION('',(#572),#18352);
#563=STYLED_ITEM('',(#18462),#572);
#572=MANIFOLD_SOLID_BREP('Body1',#6494);
#636=FACE_BOUND('',#1588,.T.);
#637=FACE_BOUND('',#1590,.T.);
#780=PLANE('',#7072);
#781=PLANE('',#7073);
#1151=FACE_OUTER_BOUND('',#1585,.T.);
#1152=FACE_OUTER_BOUND('',#1586,.T.);
#1153=FACE_OUTER_BOUND('',#1587,.T.);
#1154=FACE_OUTER_BOUND('',#1589,.T.);
#1585=EDGE_LOOP('',(#5970,#5971,#5972,#5973));
#1586=EDGE_LOOP('',(#5974,#5975,#5976,#5977));
#1587=EDGE_LOOP('',(#5978));
#1588=EDGE_LOOP('',(#5979));
#1589=EDGE_LOOP('',(#5980));
#1590=EDGE_LOOP('',(#5981));
#1993=LINE('',#18312,#2397);
#1994=LINE('',#18318,#2398);
#2397=VECTOR('',#8430,0.41);
#2398=VECTOR('',#8437,0.6);
#2562=CIRCLE('',#7067,0.41);
#2563=CIRCLE('',#7068,0.41);
#2564=CIRCLE('',#7070,0.6);
#2565=CIRCLE('',#7071,0.6);
#3167=VERTEX_POINT('',#18309);
#3168=VERTEX_POINT('',#18311);
#3169=VERTEX_POINT('',#18315);
#3170=VERTEX_POINT('',#18317);
#4102=EDGE_CURVE('',#3167,#3167,#2562,.T.);
#4103=EDGE_CURVE('',#3167,#3168,#1993,.T.);
#4104=EDGE_CURVE('',#3168,#3168,#2563,.T.);
#4105=EDGE_CURVE('',#3169,#3169,#2564,.T.);
#4106=EDGE_CURVE('',#3169,#3170,#1994,.T.);
#4107=EDGE_CURVE('',#3170,#3170,#2565,.T.);
#5970=ORIENTED_EDGE('',*,*,#4102,.F.);
#5971=ORIENTED_EDGE('',*,*,#4103,.T.);
#5972=ORIENTED_EDGE('',*,*,#4104,.T.);
#5973=ORIENTED_EDGE('',*,*,#4103,.F.);
#5974=ORIENTED_EDGE('',*,*,#4105,.F.);
#5975=ORIENTED_EDGE('',*,*,#4106,.T.);
#5976=ORIENTED_EDGE('',*,*,#4107,.T.);
#5977=ORIENTED_EDGE('',*,*,#4106,.F.);
#5978=ORIENTED_EDGE('',*,*,#4105,.T.);
#5979=ORIENTED_EDGE('',*,*,#4102,.T.);
#5980=ORIENTED_EDGE('',*,*,#4107,.F.);
#5981=ORIENTED_EDGE('',*,*,#4104,.F.);
#6111=CYLINDRICAL_SURFACE('',#7066,0.41);
#6112=CYLINDRICAL_SURFACE('',#7069,0.6);
#6482=ADVANCED_FACE('',(#1151),#6111,.F.);
#6483=ADVANCED_FACE('',(#1152),#6112,.T.);
#6484=ADVANCED_FACE('',(#1153,#636),#780,.T.);
#6485=ADVANCED_FACE('',(#1154,#637),#781,.F.);
#6494=CLOSED_SHELL('',(#6482,#6483,#6484,#6485));
#7065=AXIS2_PLACEMENT_3D('',#18307,#8424,#8425);
#7066=AXIS2_PLACEMENT_3D('',#18308,#8426,#8427);
#7067=AXIS2_PLACEMENT_3D('',#18310,#8428,#8429);
#7068=AXIS2_PLACEMENT_3D('',#18313,#8431,#8432);
#7069=AXIS2_PLACEMENT_3D('',#18314,#8433,#8434);
#7070=AXIS2_PLACEMENT_3D('',#18316,#8435,#8436);
#7071=AXIS2_PLACEMENT_3D('',#18319,#8438,#8439);
#7072=AXIS2_PLACEMENT_3D('',#18320,#8440,#8441);
#7073=AXIS2_PLACEMENT_3D('',#18321,#8442,#8443);
#8424=DIRECTION('axis',(0.,0.,1.));
#8425=DIRECTION('refdir',(1.,0.,0.));
#8426=DIRECTION('center_axis',(0.,0.,1.));
#8427=DIRECTION('ref_axis',(1.,0.,0.));
#8428=DIRECTION('center_axis',(0.,0.,-1.));
#8429=DIRECTION('ref_axis',(1.,0.,0.));
#8430=DIRECTION('',(0.,0.,-1.));
#8431=DIRECTION('center_axis',(0.,0.,-1.));
#8432=DIRECTION('ref_axis',(1.,0.,0.));
#8433=DIRECTION('center_axis',(0.,0.,1.));
#8434=DIRECTION('ref_axis',(1.,0.,0.));
#8435=DIRECTION('center_axis',(0.,0.,1.));
#8436=DIRECTION('ref_axis',(1.,0.,0.));
#8437=DIRECTION('',(0.,0.,-1.));
#8438=DIRECTION('center_axis',(0.,0.,1.));
#8439=DIRECTION('ref_axis',(1.,0.,0.));
#8440=DIRECTION('center_axis',(0.,0.,1.));
#8441=DIRECTION('ref_axis',(1.,0.,0.));
#8442=DIRECTION('center_axis',(0.,0.,1.));
#8443=DIRECTION('ref_axis',(1.,0.,0.));
#18307=CARTESIAN_POINT('',(0.,0.,0.));
#18308=CARTESIAN_POINT('Origin',(0.,0.,0.));
#18309=CARTESIAN_POINT('',(-0.41,-5.02105187650415E-17,0.1));
#18310=CARTESIAN_POINT('Origin',(0.,0.,0.1));
#18311=CARTESIAN_POINT('',(-0.41,-5.02105187650415E-17,0.));
#18312=CARTESIAN_POINT('',(-0.41,-5.02105187650415E-17,0.));
#18313=CARTESIAN_POINT('Origin',(0.,0.,0.));
#18314=CARTESIAN_POINT('Origin',(0.,0.,0.));
#18315=CARTESIAN_POINT('',(-0.6,-7.34788079488412E-17,0.1));
#18316=CARTESIAN_POINT('Origin',(0.,0.,0.1));
#18317=CARTESIAN_POINT('',(-0.6,-7.34788079488412E-17,0.));
#18318=CARTESIAN_POINT('',(-0.6,-7.34788079488412E-17,0.));
#18319=CARTESIAN_POINT('Origin',(0.,0.,0.));
#18320=CARTESIAN_POINT('Origin',(0.,0.,0.1));
#18321=CARTESIAN_POINT('Origin',(0.,0.,0.));
#18340=UNCERTAINTY_MEASURE_WITH_UNIT(LENGTH_MEASURE(0.001),#18354,
'DISTANCE_ACCURACY_VALUE',
'Maximum model space distance between geometric entities at asserted c
onnectivities');
#18341=UNCERTAINTY_MEASURE_WITH_UNIT(LENGTH_MEASURE(0.001),#18354,
'DISTANCE_ACCURACY_VALUE',
'Maximum model space distance between geometric entities at asserted c
onnectivities');
#18352=(
GEOMETRIC_REPRESENTATION_CONTEXT(3)
GLOBAL_UNCERTAINTY_ASSIGNED_CONTEXT((#18340))
GLOBAL_UNIT_ASSIGNED_CONTEXT((#18354,#18356,#18357))
REPRESENTATION_CONTEXT('','3D')
);
#18353=(
GEOMETRIC_REPRESENTATION_CONTEXT(3)
GLOBAL_UNCERTAINTY_ASSIGNED_CONTEXT((#18341))
GLOBAL_UNIT_ASSIGNED_CONTEXT((#18354,#18356,#18357))
REPRESENTATION_CONTEXT('','3D')
);
#18354=(
LENGTH_UNIT()
NAMED_UNIT(*)
SI_UNIT(.CENTI.,.METRE.)
);
#18356=(
NAMED_UNIT(*)
PLANE_ANGLE_UNIT()
SI_UNIT($,.RADIAN.)
);
#18357=(
NAMED_UNIT(*)
SI_UNIT($,.STERADIAN.)
SOLID_ANGLE_UNIT()
);
#18368=SHAPE_DEFINITION_REPRESENTATION(#18387,#18406);
#18387=PRODUCT_DEFINITION_SHAPE('',$,#18418);
#18406=SHAPE_REPRESENTATION('',(#7065),#18352);
#18407=PRODUCT_DEFINITION_CONTEXT('part definition',#18442,'design');
#18418=PRODUCT_DEFINITION('Pivot thrust washer','Pivot thrust washer',#18429,
#18407);
#18429=PRODUCT_DEFINITION_FORMATION('',$,#18454);
#18442=APPLICATION_CONTEXT(
'Core Data for Automotive Mechanical Design Process');
#18443=PRODUCT_CONTEXT('part definition',#18442,'mechanical');
#18454=PRODUCT('Pivot thrust washer','Pivot thrust washer',$,(#18443));
#18462=PRESENTATION_STYLE_ASSIGNMENT((#18470));
#18470=SURFACE_STYLE_USAGE(.BOTH.,#18478);
#18478=SURFACE_SIDE_STYLE('',(#18486));
#18486=SURFACE_STYLE_FILL_AREA(#18494);
#18494=FILL_AREA_STYLE('Washer gray',(#18502));
#18502=FILL_AREA_STYLE_COLOUR('Washer gray',#18510);
#18510=COLOUR_RGB('Washer gray',0.725490196078431,0.752941176470588,0.792156862745098);
ENDSEC;
END-ISO-10303-21;
